ISO-10303-21;
HEADER;
/* Generated by software containing ST-Developer
 * from STEP Tools, Inc. (www.steptools.com) 
 */

FILE_DESCRIPTION(
/* description */ ('Bin tilter linkage'),
/* implementation_level */ '2;1');

FILE_NAME(
/* name */ 'Bearing cap (6).step',
/* time_stamp */ '2026-10-28T03:26:24-07:00',
/* author */ (''),
/* organization */ (''),
/* preprocessor_version */ 'ST-DEVELOPER v20.2',
/* originating_system */ 'Autodesk Translation Framework v15.17.0.0',
/* authorisation */ '');

FILE_SCHEMA (('AUTOMOTIVE_DESIGN { 1 0 10303 214 3 1 1 }'));
ENDSEC;

DATA;
#10=MECHANICAL_DESIGN_GEOMETRIC_PRESENTATION_REPRESENTATION('',(#924),#23728);
#712=SHAPE_REPRESENTATION_RELATIONSHIP('SRR','None',#24178,#818);
#818=ADVANCED_BREP_SHAPE_REPRESENTATION('',(#1037),#23678);
#924=STYLED_ITEM('',(#24765),#1037);
#1037=MANIFOLD_SOLID_BREP('Body1',#12455);
#1358=FACE_BOUND('',#3394,.T.);
#1359=FACE_BOUND('',#3395,.T.);
#1360=FACE_BOUND('',#3396,.T.);
#1361=FACE_BOUND('',#3397,.T.);
#1362=FACE_BOUND('',#3398,.T.);
#1363=FACE_BOUND('',#3400,.T.);
#1364=FACE_BOUND('',#3401,.T.);
#1365=FACE_BOUND('',#3402,.T.);
#1366=FACE_BOUND('',#3403,.T.);
#1367=FACE_BOUND('',#3404,.T.);
#1709=PLANE('',#14670);
#1710=PLANE('',#14671);
#2339=FACE_OUTER_BOUND('',#3387,.T.);
#2340=FACE_OUTER_BOUND('',#3388,.T.);
#2341=FACE_OUTER_BOUND('',#3389,.T.);
#2342=FACE_OUTER_BOUND('',#3390,.T.);
#2343=FACE_OUTER_BOUND('',#3391,.T.);
#2344=FACE_OUTER_BOUND('',#3392,.T.);
#2345=FACE_OUTER_BOUND('',#3393,.T.);
#2346=FACE_OUTER_BOUND('',#3399,.T.);
#3387=EDGE_LOOP('',(#10045,#10046,#10047,#10048));
#3388=EDGE_LOOP('',(#10049,#10050,#10051,#10052));
#3389=EDGE_LOOP('',(#10053,#10054,#10055,#10056));
#3390=EDGE_LOOP('',(#10057,#10058,#10059,#10060));
#3391=EDGE_LOOP('',(#10061,#10062,#10063,#10064));
#3392=EDGE_LOOP('',(#10065,#10066,#10067,#10068));
#3393=EDGE_LOOP('',(#10069));
#3394=EDGE_LOOP('',(#10070));
#3395=EDGE_LOOP('',(#10071));
#3396=EDGE_LOOP('',(#10072));
#3397=EDGE_LOOP('',(#10073));
#3398=EDGE_LOOP('',(#10074));
#3399=EDGE_LOOP('',(#10075));
#3400=EDGE_LOOP('',(#10076));
#3401=EDGE_LOOP('',(#10077));
#3402=EDGE_LOOP('',(#10078));
#3403=EDGE_LOOP('',(#10079));
#3404=EDGE_LOOP('',(#10080));
#4225=LINE('',#21657,#4900);
#4226=LINE('',#21663,#4901);
#4227=LINE('',#21669,#4902);
#4228=LINE('',#21675,#4903);
#4229=LINE('',#21681,#4904);
#4230=LINE('',#21687,#4905);
#4900=VECTOR('',#17806,0.225000000000001);
#4901=VECTOR('',#17813,0.225000000000001);
#4902=VECTOR('',#17820,0.225000000000001);
#4903=VECTOR('',#17827,0.225000000000001);
#4904=VECTOR('',#17834,1.02);
#4905=VECTOR('',#17841,2.2);
#5659=CIRCLE('',#14653,0.225000000000001);
#5660=CIRCLE('',#14654,0.225000000000001);
#5661=CIRCLE('',#14656,0.225000000000001);
#5662=CIRCLE('',#14657,0.225000000000001);
#5663=CIRCLE('',#14659,0.225000000000001);
#5664=CIRCLE('',#14660,0.225000000000001);
#5665=CIRCLE('',#14662,0.225000000000001);
#5666=CIRCLE('',#14663,0.225000000000001);
#5667=CIRCLE('',#14665,1.02);
#5668=CIRCLE('',#14666,1.02);
#5669=CIRCLE('',#14668,2.2);
#5670=CIRCLE('',#14669,2.2);
#6513=VERTEX_POINT('',#21654);
#6514=VERTEX_POINT('',#21656);
#6515=VERTEX_POINT('',#21660);
#6516=VERTEX_POINT('',#21662);
#6517=VERTEX_POINT('',#21666);
#6518=VERTEX_POINT('',#21668);
#6519=VERTEX_POINT('',#21672);
#6520=VERTEX_POINT('',#21674);
#6521=VERTEX_POINT('',#21678);
#6522=VERTEX_POINT('',#21680);
#6523=VERTEX_POINT('',#21684);
#6524=VERTEX_POINT('',#21686);
#7762=EDGE_CURVE('',#6513,#6513,#5659,.T.);
#7763=EDGE_CURVE('',#6513,#6514,#4225,.T.);
#7764=EDGE_CURVE('',#6514,#6514,#5660,.T.);
#7765=EDGE_CURVE('',#6515,#6515,#5661,.T.);
#7766=EDGE_CURVE('',#6515,#6516,#4226,.T.);
#7767=EDGE_CURVE('',#6516,#6516,#5662,.T.);
#7768=EDGE_CURVE('',#6517,#6517,#5663,.T.);
#7769=EDGE_CURVE('',#6517,#6518,#4227,.T.);
#7770=EDGE_CURVE('',#6518,#6518,#5664,.T.);
#7771=EDGE_CURVE('',#6519,#6519,#5665,.T.);
#7772=EDGE_CURVE('',#6519,#6520,#4228,.T.);
#7773=EDGE_CURVE('',#6520,#6520,#5666,.T.);
#7774=EDGE_CURVE('',#6521,#6521,#5667,.T.);
#7775=EDGE_CURVE('',#6521,#6522,#4229,.T.);
#7776=EDGE_CURVE('',#6522,#6522,#5668,.T.);
#7777=EDGE_CURVE('',#6523,#6523,#5669,.T.);
#7778=EDGE_CURVE('',#6523,#6524,#4230,.T.);
#7779=EDGE_CURVE('',#6524,#6524,#5670,.T.);
#10045=ORIENTED_EDGE('',*,*,#7762,.F.);
#10046=ORIENTED_EDGE('',*,*,#7763,.T.);
#10047=ORIENTED_EDGE('',*,*,#7764,.F.);
#10048=ORIENTED_EDGE('',*,*,#7763,.F.);
#10049=ORIENTED_EDGE('',*,*,#7765,.F.);
#10050=ORIENTED_EDGE('',*,*,#7766,.T.);
#10051=ORIENTED_EDGE('',*,*,#7767,.F.);
#10052=ORIENTED_EDGE('',*,*,#7766,.F.);
#10053=ORIENTED_EDGE('',*,*,#7768,.F.);
#10054=ORIENTED_EDGE('',*,*,#7769,.T.);
#10055=ORIENTED_EDGE('',*,*,#7770,.F.);
#10056=ORIENTED_EDGE('',*,*,#7769,.F.);
#10057=ORIENTED_EDGE('',*,*,#7771,.F.);
#10058=ORIENTED_EDGE('',*,*,#7772,.T.);
#10059=ORIENTED_EDGE('',*,*,#7773,.F.);
#10060=ORIENTED_EDGE('',*,*,#7772,.F.);
#10061=ORIENTED_EDGE('',*,*,#7774,.F.);
#10062=ORIENTED_EDGE('',*,*,#7775,.T.);
#10063=ORIENTED_EDGE('',*,*,#7776,.T.);
#10064=ORIENTED_EDGE('',*,*,#7775,.F.);
#10065=ORIENTED_EDGE('',*,*,#7777,.F.);
#10066=ORIENTED_EDGE('',*,*,#7778,.T.);
#10067=ORIENTED_EDGE('',*,*,#7779,.T.);
#10068=ORIENTED_EDGE('',*,*,#7778,.F.);
#10069=ORIENTED_EDGE('',*,*,#7777,.T.);
#10070=ORIENTED_EDGE('',*,*,#7774,.T.);
#10071=ORIENTED_EDGE('',*,*,#7773,.T.);
#10072=ORIENTED_EDGE('',*,*,#7770,.T.);
#10073=ORIENTED_EDGE('',*,*,#7767,.T.);
#10074=ORIENTED_EDGE('',*,*,#7764,.T.);
#10075=ORIENTED_EDGE('',*,*,#7779,.F.);
#10076=ORIENTED_EDGE('',*,*,#7776,.F.);
#10077=ORIENTED_EDGE('',*,*,#7771,.T.);
#10078=ORIENTED_EDGE('',*,*,#7768,.T.);
#10079=ORIENTED_EDGE('',*,*,#7765,.T.);
#10080=ORIENTED_EDGE('',*,*,#7762,.T.);
#11495=CYLINDRICAL_SURFACE('',#14652,0.225000000000001);
#11496=CYLINDRICAL_SURFACE('',#14655,0.225000000000001);
#11497=CYLINDRICAL_SURFACE('',#14658,0.225000000000001);
#11498=CYLINDRICAL_SURFACE('',#14661,0.225000000000001);
#11499=CYLINDRICAL_SURFACE('',#14664,1.02);
#11500=CYLINDRICAL_SURFACE('',#14667,2.2);
#12064=ADVANCED_FACE('',(#2339),#11495,.F.);
#12065=ADVANCED_FACE('',(#2340),#11496,.F.);
#12066=ADVANCED_FACE('',(#2341),#11497,.F.);
#12067=ADVANCED_FACE('',(#2342),#11498,.F.);
#12068=ADVANCED_FACE('',(#2343),#11499,.F.);
#12069=ADVANCED_FACE('',(#2344),#11500,.T.);
#12070=ADVANCED_FACE('',(#2345,#1358,#1359,#1360,#1361,#1362),#1709,.T.);
#12071=ADVANCED_FACE('',(#2346,#1363,#1364,#1365,#1366,#1367),#1710,.F.);
#12455=CLOSED_SHELL('',(#12064,#12065,#12066,#12067,#12068,#12069,#12070,
#12071));
#14651=AXIS2_PLACEMENT_3D('',#21652,#17800,#17801);
#14652=AXIS2_PLACEMENT_3D('',#21653,#17802,#17803);
#14653=AXIS2_PLACEMENT_3D('',#21655,#17804,#17805);
#14654=AXIS2_PLACEMENT_3D('',#21658,#17807,#17808);
#14655=AXIS2_PLACEMENT_3D('',#21659,#17809,#17810);
#14656=AXIS2_PLACEMENT_3D('',#21661,#17811,#17812);
#14657=AXIS2_PLACEMENT_3D('',#21664,#17814,#17815);
#14658=AXIS2_PLACEMENT_3D('',#21665,#17816,#17817);
#14659=AXIS2_PLACEMENT_3D('',#21667,#17818,#17819);
#14660=AXIS2_PLACEMENT_3D('',#21670,#17821,#17822);
#14661=AXIS2_PLACEMENT_3D('',#21671,#17823,#17824);
#14662=AXIS2_PLACEMENT_3D('',#21673,#17825,#17826);
#14663=AXIS2_PLACEMENT_3D('',#21676,#17828,#17829);
#14664=AXIS2_PLACEMENT_3D('',#21677,#17830,#17831);
#14665=AXIS2_PLACEMENT_3D('',#21679,#17832,#17833);
#14666=AXIS2_PLACEMENT_3D('',#21682,#17835,#17836);
#14667=AXIS2_PLACEMENT_3D('',#21683,#17837,#17838);
#14668=AXIS2_PLACEMENT_3D('',#21685,#17839,#17840);
#14669=AXIS2_PLACEMENT_3D('',#21688,#17842,#17843);
#14670=AXIS2_PLACEMENT_3D('',#21689,#17844,#17845);
#14671=AXIS2_PLACEMENT_3D('',#21690,#17846,#17847);
#17800=DIRECTION('axis',(0.,0.,1.));
#17801=DIRECTION('refdir',(1.,0.,0.));
#17802=DIRECTION('center_axis',(0.,1.,0.));
#17803=DIRECTION('ref_axis',(1.,0.,0.));
#17804=DIRECTION('center_axis',(0.,1.,0.));
#17805=DIRECTION('ref_axis',(1.,0.,0.));
#17806=DIRECTION('',(0.,1.,0.));
#17807=DIRECTION('center_axis',(0.,-1.,0.));
#17808=DIRECTION('ref_axis',(1.,0.,0.));
#17809=DIRECTION('center_axis',(0.,1.,0.));
#17810=DIRECTION('ref_axis',(1.,0.,0.));
#17811=DIRECTION('center_axis',(0.,1.,0.));
#17812=DIRECTION('ref_axis',(1.,0.,0.));
#17813=DIRECTION('',(0.,1.,0.));
#17814=DIRECTION('center_axis',(0.,-1.,0.));
#17815=DIRECTION('ref_axis',(1.,0.,0.));
#17816=DIRECTION('center_axis',(0.,1.,0.));
#17817=DIRECTION('ref_axis',(1.,0.,0.));
#17818=DIRECTION('center_axis',(0.,1.,0.));
#17819=DIRECTION('ref_axis',(1.,0.,0.));
#17820=DIRECTION('',(0.,1.,0.));
#17821=DIRECTION('center_axis',(0.,-1.,0.));
#17822=DIRECTION('ref_axis',(1.,0.,0.));
#17823=DIRECTION('center_axis',(0.,1.,0.));
#17824=DIRECTION('ref_axis',(1.,0.,0.));
#17825=DIRECTION('center_axis',(0.,1.,0.));
#17826=DIRECTION('ref_axis',(1.,0.,0.));
#17827=DIRECTION('',(0.,1.,0.));
#17828=DIRECTION('center_axis',(0.,-1.,0.));
#17829=DIRECTION('ref_axis',(1.,0.,0.));
#17830=DIRECTION('center_axis',(0.,1.,0.));
#17831=DIRECTION('ref_axis',(1.,0.,0.));
#17832=DIRECTION('center_axis',(0.,-1.,0.));
#17833=DIRECTION('ref_axis',(1.,0.,0.));
#17834=DIRECTION('',(0.,-1.,0.));
#17835=DIRECTION('center_axis',(0.,-1.,0.));
#17836=DIRECTION('ref_axis',(1.,0.,0.));
#17837=DIRECTION('center_axis',(0.,1.,0.));
#17838=DIRECTION('ref_axis',(1.,0.,0.));
#17839=DIRECTION('center_axis',(0.,1.,0.));
#17840=DIRECTION('ref_axis',(1.,0.,0.));
#17841=DIRECTION('',(0.,-1.,0.));
#17842=DIRECTION('center_axis',(0.,1.,0.));
#17843=DIRECTION('ref_axis',(1.,0.,0.));
#17844=DIRECTION('center_axis',(0.,1.,0.));
#17845=DIRECTION('ref_axis',(1.,0.,0.));
#17846=DIRECTION('center_axis',(0.,1.,0.));
#17847=DIRECTION('ref_axis',(1.,0.,0.));
#21652=CARTESIAN_POINT('',(0.,0.,0.));
#21653=CARTESIAN_POINT('Origin',(22.893930933827,-0.9,27.3496056572921));
#21654=CARTESIAN_POINT('',(22.668930933827,-0.8,27.3496056572921));
#21655=CARTESIAN_POINT('Origin',(22.893930933827,-0.8,27.3496056572921));
#21656=CARTESIAN_POINT('',(22.668930933827,-0.5,27.3496056572921));
#21657=CARTESIAN_POINT('',(22.668930933827,-0.9,27.3496056572921));
#21658=CARTESIAN_POINT('Origin',(22.893930933827,-0.5,27.3496056572921));
#21659=CARTESIAN_POINT('Origin',(22.893930933827,-0.9,29.9659007476824));
#21660=CARTESIAN_POINT('',(22.668930933827,-0.8,29.9659007476824));
#21661=CARTESIAN_POINT('Origin',(22.893930933827,-0.8,29.9659007476824));
#21662=CARTESIAN_POINT('',(22.668930933827,-0.5,29.9659007476824));
#21663=CARTESIAN_POINT('',(22.668930933827,-0.9,29.9659007476824));
#21664=CARTESIAN_POINT('Origin',(22.893930933827,-0.5,29.9659007476824));
#21665=CARTESIAN_POINT('Origin',(25.5102260242172,-0.9,29.9659007476824));
#21666=CARTESIAN_POINT('',(25.2852260242172,-0.8,29.9659007476824));
#21667=CARTESIAN_POINT('Origin',(25.5102260242172,-0.8,29.9659007476824));
#21668=CARTESIAN_POINT('',(25.2852260242172,-0.5,29.9659007476824));
#21669=CARTESIAN_POINT('',(25.2852260242172,-0.9,29.9659007476824));
#21670=CARTESIAN_POINT('Origin',(25.5102260242172,-0.5,29.9659007476824));
#21671=CARTESIAN_POINT('Origin',(25.5102260242172,-0.9,27.3496056572921));
#21672=CARTESIAN_POINT('',(25.2852260242172,-0.8,27.3496056572921));
#21673=CARTESIAN_POINT('Origin',(25.5102260242172,-0.8,27.3496056572921));
#21674=CARTESIAN_POINT('',(25.2852260242172,-0.5,27.3496056572921));
#21675=CARTESIAN_POINT('',(25.2852260242172,-0.9,27.3496056572921));
#21676=CARTESIAN_POINT('Origin',(25.5102260242172,-0.5,27.3496056572921));
#21677=CARTESIAN_POINT('Origin',(24.2020784790221,-0.8,28.6577532024872));
#21678=CARTESIAN_POINT('',(23.1820784790221,-0.5,28.6577532024872));
#21679=CARTESIAN_POINT('Origin',(24.2020784790221,-0.5,28.6577532024872));
#21680=CARTESIAN_POINT('',(23.1820784790221,-0.8,28.6577532024872));
#21681=CARTESIAN_POINT('',(23.1820784790221,-0.8,28.6577532024872));
#21682=CARTESIAN_POINT('Origin',(24.2020784790221,-0.8,28.6577532024872));
#21683=CARTESIAN_POINT('Origin',(24.2020784790221,-0.8,28.6577532024872));
#21684=CARTESIAN_POINT('',(22.0020784790221,-0.5,28.6577532024872));
#21685=CARTESIAN_POINT('Origin',(24.2020784790221,-0.5,28.6577532024872));
#21686=CARTESIAN_POINT('',(22.0020784790221,-0.8,28.6577532024872));
#21687=CARTESIAN_POINT('',(22.0020784790221,-0.8,28.6577532024872));
#21688=CARTESIAN_POINT('Origin',(24.2020784790221,-0.8,28.6577532024872));
#21689=CARTESIAN_POINT('Origin',(24.2020784790221,-0.5,28.6577532024872));
#21690=CARTESIAN_POINT('Origin',(24.2020784790221,-0.8,28.6577532024872));
#23561=UNCERTAINTY_MEASURE_WITH_UNIT(LENGTH_MEASURE(0.001),#23729,
'DISTANCE_ACCURACY_VALUE',
'Maximum model space distance between geometric entities at asserted c
onnectivities');
#23611=UNCERTAINTY_MEASURE_WITH_UNIT(LENGTH_MEASURE(0.001),#23729,
'DISTANCE_ACCURACY_VALUE',
'Maximum model space distance between geometric entities at asserted c
onnectivities');
#23678=(
GEOMETRIC_REPRESENTATION_CONTEXT(3)
GLOBAL_UNCERTAINTY_ASSIGNED_CONTEXT((#23561))
GLOBAL_UNIT_ASSIGNED_CONTEXT((#23729,#23731,#23732))
REPRESENTATION_CONTEXT('','3D')
);
#23728=(
GEOMETRIC_REPRESENTATION_CONTEXT(3)
GLOBAL_UNCERTAINTY_ASSIGNED_CONTEXT((#23611))
GLOBAL_UNIT_ASSIGNED_CONTEXT((#23729,#23731,#23732))
REPRESENTATION_CONTEXT('','3D')
);
#23729=(
LENGTH_UNIT()
NAMED_UNIT(*)
SI_UNIT(.CENTI.,.METRE.)
);
#23731=(
NAMED_UNIT(*)
PLANE_ANGLE_UNIT()
SI_UNIT($,.RADIAN.)
);
#23732=(
NAMED_UNIT(*)
SI_UNIT($,.STERADIAN.)
SOLID_ANGLE_UNIT()
);
#23799=SHAPE_DEFINITION_REPRESENTATION(#23915,#24178);
#23915=PRODUCT_DEFINITION_SHAPE('',$,#24295);
#24178=SHAPE_REPRESENTATION('',(#14651),#23678);
#24228=PRODUCT_DEFINITION_CONTEXT('part definition',#24578,'design');
#24295=PRODUCT_DEFINITION('Bearing cap (6)','Bearing cap (6)',#24411,#24228);
#24411=PRODUCT_DEFINITION_FORMATION('',$,#24646);
#24578=APPLICATION_CONTEXT(
'Core Data for Automotive Mechanical Design Process');
#24579=PRODUCT_CONTEXT('part definition',#24578,'mechanical');
#24646=PRODUCT('Bearing cap (6)','Bearing cap (6)','Bearing cap (6)',(#24579));
#24759=COLOUR_RGB('Grey',0.48,0.52,0.57);
#24760=FILL_AREA_STYLE_COLOUR('',#24759);
#24761=FILL_AREA_STYLE('',(#24760));
#24762=SURFACE_STYLE_FILL_AREA(#24761);
#24763=SURFACE_SIDE_STYLE('',(#24762));
#24764=SURFACE_STYLE_USAGE(.BOTH.,#24763);
#24765=PRESENTATION_STYLE_ASSIGNMENT((#24764));
ENDSEC;
END-ISO-10303-21;
